ISO-10303-21;
HEADER;
/* Generated by software containing ST-Developer
 * from STEP Tools, Inc. (www.steptools.com) 
 */

FILE_DESCRIPTION(
/* description */ ('Ratchet and pawl hand winch drum'),
/* implementation_level */ '2;1');

FILE_NAME(
/* name */ 'M4x10 Cap Screw.step',
/* time_stamp */ '2026-10-27T12:42:58-07:00',
/* author */ (''),
/* organization */ (''),
/* preprocessor_version */ 'ST-DEVELOPER v20.2',
/* originating_system */ 'Autodesk Translation Framework v15.17.0.0',
/* authorisation */ '');

FILE_SCHEMA (('AUTOMOTIVE_DESIGN { 1 0 10303 214 3 1 1 }'));
ENDSEC;

DATA;
#10=MECHANICAL_DESIGN_GEOMETRIC_PRESENTATION_REPRESENTATION('',(#409),#11801);
#14=CONICAL_SURFACE('',#7038,0.325,0.785398163397448);
#15=CONICAL_SURFACE('',#7042,0.335,0.785398163397448);
#16=CONICAL_SURFACE('',#7046,0.21,0.463647609000806);
#24=ORIENTED_CLOSED_SHELL('',*,#6287,.F.);
#27=BREP_WITH_VOIDS('Body1',#6288,(#24));
#340=SHAPE_REPRESENTATION_RELATIONSHIP('SRR','None',#11967,#374);
#374=ADVANCED_BREP_SHAPE_REPRESENTATION('',(#27),#11784);
#409=STYLED_ITEM('',(#12220),#27);
#563=FACE_BOUND('',#1504,.T.);
#715=PLANE('',#7026);
#716=PLANE('',#7027);
#717=PLANE('',#7028);
#718=PLANE('',#7029);
#719=PLANE('',#7030);
#720=PLANE('',#7031);
#721=PLANE('',#7032);
#722=PLANE('',#7033);
#723=PLANE('',#7034);
#724=PLANE('',#7036);
#725=PLANE('',#7044);
#1027=FACE_OUTER_BOUND('',#1490,.T.);
#1028=FACE_OUTER_BOUND('',#1491,.T.);
#1029=FACE_OUTER_BOUND('',#1492,.T.);
#1030=FACE_OUTER_BOUND('',#1493,.T.);
#1031=FACE_OUTER_BOUND('',#1494,.T.);
#1032=FACE_OUTER_BOUND('',#1495,.T.);
#1033=FACE_OUTER_BOUND('',#1496,.T.);
#1034=FACE_OUTER_BOUND('',#1497,.T.);
#1035=FACE_OUTER_BOUND('',#1498,.T.);
#1036=FACE_OUTER_BOUND('',#1499,.T.);
#1037=FACE_OUTER_BOUND('',#1500,.T.);
#1038=FACE_OUTER_BOUND('',#1501,.T.);
#1039=FACE_OUTER_BOUND('',#1502,.T.);
#1040=FACE_OUTER_BOUND('',#1503,.T.);
#1041=FACE_OUTER_BOUND('',#1505,.T.);
#1042=FACE_OUTER_BOUND('',#1506,.T.);
#1490=EDGE_LOOP('',(#5041,#5042,#5043,#5044));
#1491=EDGE_LOOP('',(#5045,#5046,#5047,#5048));
#1492=EDGE_LOOP('',(#5049,#5050,#5051,#5052));
#1493=EDGE_LOOP('',(#5053,#5054,#5055,#5056));
#1494=EDGE_LOOP('',(#5057,#5058,#5059,#5060));
#1495=EDGE_LOOP('',(#5061,#5062,#5063,#5064));
#1496=EDGE_LOOP('',(#5065,#5066,#5067,#5068,#5069,#5070));
#1497=EDGE_LOOP('',(#5071,#5072,#5073,#5074,#5075,#5076));
#1498=EDGE_LOOP('',(#5077));
#1499=EDGE_LOOP('',(#5078));
#1500=EDGE_LOOP('',(#5079,#5080,#5081,#5082));
#1501=EDGE_LOOP('',(#5083,#5084,#5085,#5086));
#1502=EDGE_LOOP('',(#5087,#5088,#5089,#5090));
#1503=EDGE_LOOP('',(#5091));
#1504=EDGE_LOOP('',(#5092));
#1505=EDGE_LOOP('',(#5093,#5094,#5095,#5096));
#1506=EDGE_LOOP('',(#5097,#5098,#5099,#5100));
#1935=LINE('',#10518,#2446);
#1936=LINE('',#10520,#2447);
#1937=LINE('',#10522,#2448);
#1938=LINE('',#10523,#2449);
#1939=LINE('',#10526,#2450);
#1940=LINE('',#10528,#2451);
#1941=LINE('',#10529,#2452);
#1942=LINE('',#10532,#2453);
#1943=LINE('',#10534,#2454);
#1944=LINE('',#10535,#2455);
#1945=LINE('',#10538,#2456);
#1946=LINE('',#10540,#2457);
#1947=LINE('',#10541,#2458);
#1948=LINE('',#10544,#2459);
#1949=LINE('',#10546,#2460);
#1950=LINE('',#10547,#2461);
#1951=LINE('',#10549,#2462);
#1952=LINE('',#10550,#2463);
#1953=LINE('',#10562,#2464);
#1954=LINE('',#10566,#2465);
#1955=LINE('',#10570,#2466);
#1956=LINE('',#10577,#2467);
#1957=LINE('',#10579,#2468);
#2446=VECTOR('',#8292,1.);
#2447=VECTOR('',#8293,1.);
#2448=VECTOR('',#8294,1.);
#2449=VECTOR('',#8295,1.);
#2450=VECTOR('',#8298,1.);
#2451=VECTOR('',#8299,1.);
#2452=VECTOR('',#8300,1.);
#2453=VECTOR('',#8303,1.);
#2454=VECTOR('',#8304,1.);
#2455=VECTOR('',#8305,1.);
#2456=VECTOR('',#8308,1.);
#2457=VECTOR('',#8309,1.);
#2458=VECTOR('',#8310,1.);
#2459=VECTOR('',#8313,1.);
#2460=VECTOR('',#8314,1.);
#2461=VECTOR('',#8315,1.);
#2462=VECTOR('',#8318,1.);
#2463=VECTOR('',#8319,1.);
#2464=VECTOR('',#8336,0.325);
#2465=VECTOR('',#8341,0.35);
#2466=VECTOR('',#8346,0.335);
#2467=VECTOR('',#8355,0.21);
#2468=VECTOR('',#8358,0.2);
#2854=CIRCLE('',#7035,0.1954);
#2855=CIRCLE('',#7037,0.3);
#2856=CIRCLE('',#7039,0.35);
#2857=CIRCLE('',#7041,0.35);
#2858=CIRCLE('',#7043,0.32);
#2859=CIRCLE('',#7045,0.22);
#2860=CIRCLE('',#7047,0.1954);
#3213=VERTEX_POINT('',#10516);
#3214=VERTEX_POINT('',#10517);
#3215=VERTEX_POINT('',#10519);
#3216=VERTEX_POINT('',#10521);
#3217=VERTEX_POINT('',#10525);
#3218=VERTEX_POINT('',#10527);
#3219=VERTEX_POINT('',#10531);
#3220=VERTEX_POINT('',#10533);
#3221=VERTEX_POINT('',#10537);
#3222=VERTEX_POINT('',#10539);
#3223=VERTEX_POINT('',#10543);
#3224=VERTEX_POINT('',#10545);
#3225=VERTEX_POINT('',#10554);
#3226=VERTEX_POINT('',#10557);
#3227=VERTEX_POINT('',#10560);
#3228=VERTEX_POINT('',#10564);
#3229=VERTEX_POINT('',#10568);
#3230=VERTEX_POINT('',#10572);
#3231=VERTEX_POINT('',#10575);
#3864=EDGE_CURVE('',#3213,#3214,#1935,.T.);
#3865=EDGE_CURVE('',#3214,#3215,#1936,.T.);
#3866=EDGE_CURVE('',#3215,#3216,#1937,.T.);
#3867=EDGE_CURVE('',#3213,#3216,#1938,.T.);
#3868=EDGE_CURVE('',#3214,#3217,#1939,.T.);
#3869=EDGE_CURVE('',#3217,#3218,#1940,.T.);
#3870=EDGE_CURVE('',#3218,#3215,#1941,.T.);
#3871=EDGE_CURVE('',#3217,#3219,#1942,.T.);
#3872=EDGE_CURVE('',#3219,#3220,#1943,.T.);
#3873=EDGE_CURVE('',#3220,#3218,#1944,.T.);
#3874=EDGE_CURVE('',#3219,#3221,#1945,.T.);
#3875=EDGE_CURVE('',#3221,#3222,#1946,.T.);
#3876=EDGE_CURVE('',#3222,#3220,#1947,.T.);
#3877=EDGE_CURVE('',#3221,#3223,#1948,.T.);
#3878=EDGE_CURVE('',#3223,#3224,#1949,.T.);
#3879=EDGE_CURVE('',#3224,#3222,#1950,.T.);
#3880=EDGE_CURVE('',#3223,#3213,#1951,.T.);
#3881=EDGE_CURVE('',#3216,#3224,#1952,.T.);
#3882=EDGE_CURVE('',#3225,#3225,#2854,.T.);
#3883=EDGE_CURVE('',#3226,#3226,#2855,.T.);
#3884=EDGE_CURVE('',#3227,#3227,#2856,.T.);
#3885=EDGE_CURVE('',#3227,#3226,#1953,.T.);
#3886=EDGE_CURVE('',#3228,#3228,#2857,.T.);
#3887=EDGE_CURVE('',#3228,#3227,#1954,.T.);
#3888=EDGE_CURVE('',#3229,#3229,#2858,.T.);
#3889=EDGE_CURVE('',#3229,#3228,#1955,.T.);
#3890=EDGE_CURVE('',#3230,#3230,#2859,.T.);
#3891=EDGE_CURVE('',#3231,#3231,#2860,.F.);
#3892=EDGE_CURVE('',#3231,#3230,#1956,.T.);
#3893=EDGE_CURVE('',#3225,#3231,#1957,.T.);
#5041=ORIENTED_EDGE('',*,*,#3864,.T.);
#5042=ORIENTED_EDGE('',*,*,#3865,.T.);
#5043=ORIENTED_EDGE('',*,*,#3866,.T.);
#5044=ORIENTED_EDGE('',*,*,#3867,.F.);
#5045=ORIENTED_EDGE('',*,*,#3868,.T.);
#5046=ORIENTED_EDGE('',*,*,#3869,.T.);
#5047=ORIENTED_EDGE('',*,*,#3870,.T.);
#5048=ORIENTED_EDGE('',*,*,#3865,.F.);
#5049=ORIENTED_EDGE('',*,*,#3871,.T.);
#5050=ORIENTED_EDGE('',*,*,#3872,.T.);
#5051=ORIENTED_EDGE('',*,*,#3873,.T.);
#5052=ORIENTED_EDGE('',*,*,#3869,.F.);
#5053=ORIENTED_EDGE('',*,*,#3874,.T.);
#5054=ORIENTED_EDGE('',*,*,#3875,.T.);
#5055=ORIENTED_EDGE('',*,*,#3876,.T.);
#5056=ORIENTED_EDGE('',*,*,#3872,.F.);
#5057=ORIENTED_EDGE('',*,*,#3877,.T.);
#5058=ORIENTED_EDGE('',*,*,#3878,.T.);
#5059=ORIENTED_EDGE('',*,*,#3879,.T.);
#5060=ORIENTED_EDGE('',*,*,#3875,.F.);
#5061=ORIENTED_EDGE('',*,*,#3880,.T.);
#5062=ORIENTED_EDGE('',*,*,#3867,.T.);
#5063=ORIENTED_EDGE('',*,*,#3881,.T.);
#5064=ORIENTED_EDGE('',*,*,#3878,.F.);
#5065=ORIENTED_EDGE('',*,*,#3880,.F.);
#5066=ORIENTED_EDGE('',*,*,#3877,.F.);
#5067=ORIENTED_EDGE('',*,*,#3874,.F.);
#5068=ORIENTED_EDGE('',*,*,#3871,.F.);
#5069=ORIENTED_EDGE('',*,*,#3868,.F.);
#5070=ORIENTED_EDGE('',*,*,#3864,.F.);
#5071=ORIENTED_EDGE('',*,*,#3881,.F.);
#5072=ORIENTED_EDGE('',*,*,#3866,.F.);
#5073=ORIENTED_EDGE('',*,*,#3870,.F.);
#5074=ORIENTED_EDGE('',*,*,#3873,.F.);
#5075=ORIENTED_EDGE('',*,*,#3876,.F.);
#5076=ORIENTED_EDGE('',*,*,#3879,.F.);
#5077=ORIENTED_EDGE('',*,*,#3882,.F.);
#5078=ORIENTED_EDGE('',*,*,#3883,.F.);
#5079=ORIENTED_EDGE('',*,*,#3884,.F.);
#5080=ORIENTED_EDGE('',*,*,#3885,.T.);
#5081=ORIENTED_EDGE('',*,*,#3883,.T.);
#5082=ORIENTED_EDGE('',*,*,#3885,.F.);
#5083=ORIENTED_EDGE('',*,*,#3886,.F.);
#5084=ORIENTED_EDGE('',*,*,#3887,.T.);
#5085=ORIENTED_EDGE('',*,*,#3884,.T.);
#5086=ORIENTED_EDGE('',*,*,#3887,.F.);
#5087=ORIENTED_EDGE('',*,*,#3888,.F.);
#5088=ORIENTED_EDGE('',*,*,#3889,.T.);
#5089=ORIENTED_EDGE('',*,*,#3886,.T.);
#5090=ORIENTED_EDGE('',*,*,#3889,.F.);
#5091=ORIENTED_EDGE('',*,*,#3888,.T.);
#5092=ORIENTED_EDGE('',*,*,#3890,.F.);
#5093=ORIENTED_EDGE('',*,*,#3891,.F.);
#5094=ORIENTED_EDGE('',*,*,#3892,.T.);
#5095=ORIENTED_EDGE('',*,*,#3890,.T.);
#5096=ORIENTED_EDGE('',*,*,#3892,.F.);
#5097=ORIENTED_EDGE('',*,*,#3882,.T.);
#5098=ORIENTED_EDGE('',*,*,#3893,.T.);
#5099=ORIENTED_EDGE('',*,*,#3891,.T.);
#5100=ORIENTED_EDGE('',*,*,#3893,.F.);
#5875=CYLINDRICAL_SURFACE('',#7040,0.35);
#5876=CYLINDRICAL_SURFACE('',#7048,0.1954);
#6097=ADVANCED_FACE('',(#1027),#715,.F.);
#6098=ADVANCED_FACE('',(#1028),#716,.F.);
#6099=ADVANCED_FACE('',(#1029),#717,.F.);
#6100=ADVANCED_FACE('',(#1030),#718,.F.);
#6101=ADVANCED_FACE('',(#1031),#719,.F.);
#6102=ADVANCED_FACE('',(#1032),#720,.F.);
#6103=ADVANCED_FACE('',(#1033),#721,.F.);
#6104=ADVANCED_FACE('',(#1034),#722,.F.);
#6105=ADVANCED_FACE('',(#1035),#723,.F.);
#6106=ADVANCED_FACE('',(#1036),#724,.T.);
#6107=ADVANCED_FACE('',(#1037),#14,.T.);
#6108=ADVANCED_FACE('',(#1038),#5875,.T.);
#6109=ADVANCED_FACE('',(#1039),#15,.T.);
#6110=ADVANCED_FACE('',(#1040,#563),#725,.T.);
#6111=ADVANCED_FACE('',(#1041),#16,.T.);
#6112=ADVANCED_FACE('',(#1042),#5876,.T.);
#6287=CLOSED_SHELL('',(#6097,#6098,#6099,#6100,#6101,#6102,#6103,#6104));
#6288=CLOSED_SHELL('',(#6105,#6106,#6107,#6108,#6109,#6110,#6111,#6112));
#7025=AXIS2_PLACEMENT_3D('',#10514,#8288,#8289);
#7026=AXIS2_PLACEMENT_3D('',#10515,#8290,#8291);
#7027=AXIS2_PLACEMENT_3D('',#10524,#8296,#8297);
#7028=AXIS2_PLACEMENT_3D('',#10530,#8301,#8302);
#7029=AXIS2_PLACEMENT_3D('',#10536,#8306,#8307);
#7030=AXIS2_PLACEMENT_3D('',#10542,#8311,#8312);
#7031=AXIS2_PLACEMENT_3D('',#10548,#8316,#8317);
#7032=AXIS2_PLACEMENT_3D('',#10551,#8320,#8321);
#7033=AXIS2_PLACEMENT_3D('',#10552,#8322,#8323);
#7034=AXIS2_PLACEMENT_3D('',#10553,#8324,#8325);
#7035=AXIS2_PLACEMENT_3D('',#10555,#8326,#8327);
#7036=AXIS2_PLACEMENT_3D('',#10556,#8328,#8329);
#7037=AXIS2_PLACEMENT_3D('',#10558,#8330,#8331);
#7038=AXIS2_PLACEMENT_3D('',#10559,#8332,#8333);
#7039=AXIS2_PLACEMENT_3D('',#10561,#8334,#8335);
#7040=AXIS2_PLACEMENT_3D('',#10563,#8337,#8338);
#7041=AXIS2_PLACEMENT_3D('',#10565,#8339,#8340);
#7042=AXIS2_PLACEMENT_3D('',#10567,#8342,#8343);
#7043=AXIS2_PLACEMENT_3D('',#10569,#8344,#8345);
#7044=AXIS2_PLACEMENT_3D('',#10571,#8347,#8348);
#7045=AXIS2_PLACEMENT_3D('',#10573,#8349,#8350);
#7046=AXIS2_PLACEMENT_3D('',#10574,#8351,#8352);
#7047=AXIS2_PLACEMENT_3D('',#10576,#8353,#8354);
#7048=AXIS2_PLACEMENT_3D('',#10578,#8356,#8357);
#8288=DIRECTION('axis',(0.,0.,1.));
#8289=DIRECTION('refdir',(1.,0.,0.));
#8290=DIRECTION('center_axis',(0.866025403784439,0.,-0.5));
#8291=DIRECTION('ref_axis',(0.5,0.,0.866025403784439));
#8292=DIRECTION('',(-0.5,0.,-0.866025403784439));
#8293=DIRECTION('',(0.,-1.,0.));
#8294=DIRECTION('',(0.5,0.,0.866025403784439));
#8295=DIRECTION('',(0.,-1.,0.));
#8296=DIRECTION('center_axis',(1.60246890531964E-16,0.,-1.));
#8297=DIRECTION('ref_axis',(1.,0.,1.60246890531964E-16));
#8298=DIRECTION('',(-1.,0.,-1.60246890531964E-16));
#8299=DIRECTION('',(0.,-1.,0.));
#8300=DIRECTION('',(1.,0.,1.60246890531964E-16));
#8301=DIRECTION('center_axis',(-0.866025403784439,0.,-0.5));
#8302=DIRECTION('ref_axis',(0.5,0.,-0.866025403784439));
#8303=DIRECTION('',(-0.5,0.,0.866025403784439));
#8304=DIRECTION('',(0.,-1.,0.));
#8305=DIRECTION('',(0.5,0.,-0.866025403784439));
#8306=DIRECTION('center_axis',(-0.866025403784439,0.,0.5));
#8307=DIRECTION('ref_axis',(-0.5,0.,-0.866025403784439));
#8308=DIRECTION('',(0.5,0.,0.866025403784439));
#8309=DIRECTION('',(0.,-1.,0.));
#8310=DIRECTION('',(-0.5,0.,-0.866025403784439));
#8311=DIRECTION('center_axis',(-1.60246890531964E-16,0.,1.));
#8312=DIRECTION('ref_axis',(-1.,0.,-1.60246890531964E-16));
#8313=DIRECTION('',(1.,0.,1.60246890531964E-16));
#8314=DIRECTION('',(0.,-1.,0.));
#8315=DIRECTION('',(-1.,0.,-1.60246890531964E-16));
#8316=DIRECTION('center_axis',(0.866025403784439,0.,0.5));
#8317=DIRECTION('ref_axis',(-0.5,0.,0.866025403784439));
#8318=DIRECTION('',(0.5,0.,-0.866025403784439));
#8319=DIRECTION('',(-0.5,0.,0.866025403784439));
#8320=DIRECTION('center_axis',(0.,1.,0.));
#8321=DIRECTION('ref_axis',(1.,0.,0.));
#8322=DIRECTION('center_axis',(0.,-1.,0.));
#8323=DIRECTION('ref_axis',(0.,0.,-1.));
#8324=DIRECTION('center_axis',(0.,1.,0.));
#8325=DIRECTION('ref_axis',(1.,0.,0.));
#8326=DIRECTION('center_axis',(0.,1.,0.));
#8327=DIRECTION('ref_axis',(1.,0.,0.));
#8328=DIRECTION('center_axis',(0.,1.,0.));
#8329=DIRECTION('ref_axis',(0.,0.,1.));
#8330=DIRECTION('center_axis',(0.,-1.,0.));
#8331=DIRECTION('ref_axis',(1.,0.,0.));
#8332=DIRECTION('center_axis',(0.,-1.,0.));
#8333=DIRECTION('ref_axis',(1.,0.,0.));
#8334=DIRECTION('center_axis',(0.,-1.,0.));
#8335=DIRECTION('ref_axis',(1.,0.,0.));
#8336=DIRECTION('',(0.707106781186547,0.707106781186548,8.65956056235493E-17));
#8337=DIRECTION('center_axis',(0.,-1.,0.));
#8338=DIRECTION('ref_axis',(1.,0.,0.));
#8339=DIRECTION('center_axis',(0.,-1.,0.));
#8340=DIRECTION('ref_axis',(1.,0.,0.));
#8341=DIRECTION('',(0.,1.,0.));
#8342=DIRECTION('center_axis',(0.,1.,0.));
#8343=DIRECTION('ref_axis',(1.,0.,0.));
#8344=DIRECTION('center_axis',(0.,-1.,0.));
#8345=DIRECTION('ref_axis',(1.,0.,0.));
#8346=DIRECTION('',(-0.707106781186547,0.707106781186548,-8.65956056235493E-17));
#8347=DIRECTION('center_axis',(0.,-1.,0.));
#8348=DIRECTION('ref_axis',(0.,0.,-1.));
#8349=DIRECTION('center_axis',(0.,-1.,0.));
#8350=DIRECTION('ref_axis',(1.,0.,0.));
#8351=DIRECTION('center_axis',(0.,1.,0.));
#8352=DIRECTION('ref_axis',(1.,0.,0.));
#8353=DIRECTION('center_axis',(0.,1.,0.));
#8354=DIRECTION('ref_axis',(1.,0.,0.));
#8355=DIRECTION('',(-0.447213595499958,0.894427190999916,-5.47678698264203E-17));
#8356=DIRECTION('center_axis',(0.,-1.,0.));
#8357=DIRECTION('ref_axis',(1.,0.,0.));
#8358=DIRECTION('',(0.,1.,0.));
#10514=CARTESIAN_POINT('',(0.,0.,0.));
#10515=CARTESIAN_POINT('Origin',(0.0866025403784439,-0.4,-0.15));
#10516=CARTESIAN_POINT('',(0.173205080756888,-0.4,0.));
#10517=CARTESIAN_POINT('',(0.0866025403784439,-0.4,-0.15));
#10518=CARTESIAN_POINT('',(0.173205080756888,-0.4,0.));
#10519=CARTESIAN_POINT('',(0.0866025403784439,-0.64,-0.15));
#10520=CARTESIAN_POINT('',(0.0866025403784439,-0.4,-0.15));
#10521=CARTESIAN_POINT('',(0.173205080756888,-0.64,0.));
#10522=CARTESIAN_POINT('',(0.173205080756888,-0.64,0.));
#10523=CARTESIAN_POINT('',(0.173205080756888,-0.4,0.));
#10524=CARTESIAN_POINT('Origin',(-0.0866025403784438,-0.4,-0.15));
#10525=CARTESIAN_POINT('',(-0.0866025403784438,-0.4,-0.15));
#10526=CARTESIAN_POINT('',(0.0866025403784439,-0.4,-0.15));
#10527=CARTESIAN_POINT('',(-0.0866025403784438,-0.64,-0.15));
#10528=CARTESIAN_POINT('',(-0.0866025403784438,-0.4,-0.15));
#10529=CARTESIAN_POINT('',(0.0866025403784439,-0.64,-0.15));
#10530=CARTESIAN_POINT('Origin',(-0.173205080756888,-0.4,-2.77555756156289E-17));
#10531=CARTESIAN_POINT('',(-0.173205080756888,-0.4,-2.12115047744981E-17));
#10532=CARTESIAN_POINT('',(-0.0866025403784438,-0.4,-0.15));
#10533=CARTESIAN_POINT('',(-0.173205080756888,-0.64,-2.77555756156289E-17));
#10534=CARTESIAN_POINT('',(-0.173205080756888,-0.4,-2.12115047744981E-17));
#10535=CARTESIAN_POINT('',(-0.0866025403784438,-0.64,-0.15));
#10536=CARTESIAN_POINT('Origin',(-0.0866025403784439,-0.4,0.15));
#10537=CARTESIAN_POINT('',(-0.0866025403784439,-0.4,0.15));
#10538=CARTESIAN_POINT('',(-0.173205080756888,-0.4,-2.12115047744981E-17));
#10539=CARTESIAN_POINT('',(-0.0866025403784439,-0.64,0.15));
#10540=CARTESIAN_POINT('',(-0.0866025403784439,-0.4,0.15));
#10541=CARTESIAN_POINT('',(-0.173205080756888,-0.64,-2.12115047744981E-17));
#10542=CARTESIAN_POINT('Origin',(0.0866025403784439,-0.4,0.15));
#10543=CARTESIAN_POINT('',(0.0866025403784439,-0.4,0.15));
#10544=CARTESIAN_POINT('',(-0.0866025403784439,-0.4,0.15));
#10545=CARTESIAN_POINT('',(0.0866025403784439,-0.64,0.15));
#10546=CARTESIAN_POINT('',(0.0866025403784439,-0.4,0.15));
#10547=CARTESIAN_POINT('',(-0.0866025403784439,-0.64,0.15));
#10548=CARTESIAN_POINT('Origin',(0.173205080756888,-0.4,0.));
#10549=CARTESIAN_POINT('',(0.0866025403784439,-0.4,0.15));
#10550=CARTESIAN_POINT('',(0.0866025403784439,-0.64,0.15));
#10551=CARTESIAN_POINT('Origin',(0.,-0.4,-2.77555756156289E-17));
#10552=CARTESIAN_POINT('Origin',(0.,-0.64,-2.77555756156289E-17));
#10553=CARTESIAN_POINT('Origin',(0.,-1.,0.));
#10554=CARTESIAN_POINT('',(-0.1954,-1.,2.39295984553393E-17));
#10555=CARTESIAN_POINT('Origin',(0.,-1.,0.));
#10556=CARTESIAN_POINT('Origin',(0.3,0.4,0.));
#10557=CARTESIAN_POINT('',(-0.3,0.4,-3.67394039744206E-17));
#10558=CARTESIAN_POINT('Origin',(0.,0.4,0.));
#10559=CARTESIAN_POINT('Origin',(0.,0.375,0.));
#10560=CARTESIAN_POINT('',(-0.35,0.35,-4.28626379701573E-17));
#10561=CARTESIAN_POINT('Origin',(0.,0.35,0.));
#10562=CARTESIAN_POINT('',(-0.325,0.375,-3.9801020972289E-17));
#10563=CARTESIAN_POINT('Origin',(0.,0.19,0.));
#10564=CARTESIAN_POINT('',(-0.35,0.03,-4.28626379701574E-17));
#10565=CARTESIAN_POINT('Origin',(0.,0.03,0.));
#10566=CARTESIAN_POINT('',(-0.35,0.19,-4.28626379701574E-17));
#10567=CARTESIAN_POINT('Origin',(0.,0.0149999999999999,0.));
#10568=CARTESIAN_POINT('',(-0.32,-3.29597460435593E-17,-3.91886975727153E-17));
#10569=CARTESIAN_POINT('Origin',(0.,0.,0.));
#10570=CARTESIAN_POINT('',(-0.335,0.0149999999999999,-4.10256677714363E-17));
#10571=CARTESIAN_POINT('Origin',(0.22,0.,0.));
#10572=CARTESIAN_POINT('',(-0.22,-6.93889390390723E-18,-2.69422295812418E-17));
#10573=CARTESIAN_POINT('Origin',(0.,0.,0.));
#10574=CARTESIAN_POINT('Origin',(0.,-0.02,0.));
#10575=CARTESIAN_POINT('',(-0.1954,-0.0492,2.39295984553393E-17));
#10576=CARTESIAN_POINT('Origin',(0.,-0.0492,0.));
#10577=CARTESIAN_POINT('',(-0.21,-0.02,-2.57175827820944E-17));
#10578=CARTESIAN_POINT('Origin',(0.,-0.8,0.));
#10579=CARTESIAN_POINT('',(-0.1954,-0.8,-2.39295984553393E-17));
#11744=UNCERTAINTY_MEASURE_WITH_UNIT(LENGTH_MEASURE(0.001),#11802,
'DISTANCE_ACCURACY_VALUE',
'Maximum model space distance between geometric entities at asserted c
onnectivities');
#11761=UNCERTAINTY_MEASURE_WITH_UNIT(LENGTH_MEASURE(0.001),#11802,
'DISTANCE_ACCURACY_VALUE',
'Maximum model space distance between geometric entities at asserted c
onnectivities');
#11784=(
GEOMETRIC_REPRESENTATION_CONTEXT(3)
GLOBAL_UNCERTAINTY_ASSIGNED_CONTEXT((#11744))
GLOBAL_UNIT_ASSIGNED_CONTEXT((#11802,#11804,#11805))
REPRESENTATION_CONTEXT('','3D')
);
#11801=(
GEOMETRIC_REPRESENTATION_CONTEXT(3)
GLOBAL_UNCERTAINTY_ASSIGNED_CONTEXT((#11761))
GLOBAL_UNIT_ASSIGNED_CONTEXT((#11802,#11804,#11805))
REPRESENTATION_CONTEXT('','3D')
);
#11802=(
LENGTH_UNIT()
NAMED_UNIT(*)
SI_UNIT(.CENTI.,.METRE.)
);
#11804=(
NAMED_UNIT(*)
PLANE_ANGLE_UNIT()
SI_UNIT($,.RADIAN.)
);
#11805=(
NAMED_UNIT(*)
SI_UNIT($,.STERADIAN.)
SOLID_ANGLE_UNIT()
);
#11828=SHAPE_DEFINITION_REPRESENTATION(#11869,#11967);
#11869=PRODUCT_DEFINITION_SHAPE('',$,#12007);
#11967=SHAPE_REPRESENTATION('',(#7025),#11784);
#11984=PRODUCT_DEFINITION_CONTEXT('part definition',#12103,'design');
#12007=PRODUCT_DEFINITION('M4x10 Cap Screw','M4x10 Cap Screw',#12046,#11984);
#12046=PRODUCT_DEFINITION_FORMATION('',$,#12127);
#12103=APPLICATION_CONTEXT(
'Core Data for Automotive Mechanical Design Process');
#12104=PRODUCT_CONTEXT('part definition',#12103,'mechanical');
#12127=PRODUCT('M4x10 Cap Screw','M4x10 Cap Screw','M4x10 Cap Screw',(#12104));
#12214=COLOUR_RGB('Black',0.12,0.14,0.17);
#12215=FILL_AREA_STYLE_COLOUR('',#12214);
#12216=FILL_AREA_STYLE('',(#12215));
#12217=SURFACE_STYLE_FILL_AREA(#12216);
#12218=SURFACE_SIDE_STYLE('',(#12217));
#12219=SURFACE_STYLE_USAGE(.BOTH.,#12218);
#12220=PRESENTATION_STYLE_ASSIGNMENT((#12219));
ENDSEC;
END-ISO-10303-21;
